ISO-10303-21;
HEADER;
FILE_DESCRIPTION (('STEP AP214'),
    '1' );
FILE_NAME ('Part1.step',
    '2026-10-09T17:48:21',
    ( '' ),
    ( '' ),
    'SwSTEP 2.0',
    'SolidWorks 2024',
    '' );
FILE_SCHEMA (( 'AUTOMOTIVE_DESIGN' ));
ENDSEC;

DATA;
#24=CARTESIAN_POINT ( 'NONE',  ( 4.573385150445044900, -19.31989681812820692, 6.000000000000000000 ) ) ;
#46=CARTESIAN_POINT ( 'NONE',  ( 3.469446951953614189E-15, -24.00000000000000000, 0.000000000000000000 ) ) ;
#74=VECTOR ( 'NONE', #15192, 1000.000000000000000 ) ;
#126=STYLED_ITEM ( 'NONE', ( #12347 ), #5610 ) ;
#142=DIRECTION ( 'NONE',  ( 1.000000000000000000, 0.000000000000000000, 0.000000000000000000 ) ) ;
#157=EDGE_LOOP ( 'NONE', ( #11724, #9065, #934, #14643 ) ) ;
#168=AXIS2_PLACEMENT_3D ( 'NONE', #2465, #7215, #142 ) ;
#236=DIRECTION ( 'NONE',  ( -0.000000000000000000, 0.000000000000000000, 1.000000000000000000 ) ) ;
#263=VERTEX_POINT ( 'NONE', #12551 ) ;
#285=AXIS2_PLACEMENT_3D ( 'NONE', #3423, #3496, #1409 ) ;
#297=EDGE_LOOP ( 'NONE', ( #2095, #11678 ) ) ;
#397=FACE_OUTER_BOUND ( 'NONE', #157, .T. ) ;
#398=EDGE_CURVE ( 'NONE', #12114, #15067, #14313, .T. ) ;
#404=CARTESIAN_POINT ( 'NONE',  ( 40.52020888806953991, -24.00000000000000000, 0.000000000000000000 ) ) ;
#406=CIRCLE ( 'NONE', #9069, 1.999999999999988010 ) ;
#430=EDGE_CURVE ( 'NONE', #12493, #12176, #14014, .T. ) ;
#435=EDGE_LOOP ( 'NONE', ( #14703, #1208, #1894, #9439 ) ) ;
#452=CIRCLE ( 'NONE', #10103, 1.999999999999988010 ) ;
#461=CARTESIAN_POINT ( 'NONE',  ( 3.469446951953614189E-15, -24.00000000000000000, 6.000000000000000000 ) ) ;
#477=DIRECTION ( 'NONE',  ( -0.000000000000000000, -0.000000000000000000, 1.000000000000000000 ) ) ;
#586=CARTESIAN_POINT ( 'NONE',  ( 0.000000000000000000, 0.000000000000000000, 6.000000000000000000 ) ) ;
#599=DIRECTION ( 'NONE',  ( 0.000000000000000000, 1.000000000000000000, 0.000000000000000000 ) ) ;
#628=ORIENTED_EDGE ( 'NONE', *, *, #8187, .F. ) ;
#713=EDGE_CURVE ( 'NONE', #10232, #13570, #9817, .T. ) ;
#726=VERTEX_POINT ( 'NONE', #404 ) ;
#766=CARTESIAN_POINT ( 'NONE',  ( 35.35543536254876074, -3.618985300545107364, 6.000000000000000000 ) ) ;
#820=ORIENTED_EDGE ( 'NONE', *, *, #1709, .T. ) ;
#828=DIRECTION ( 'NONE',  ( -0.000000000000000000, -0.000000000000000000, 1.000000000000000000 ) ) ;
#843=DIRECTION ( 'NONE',  ( -0.000000000000000000, 1.000000000000000000, -0.000000000000000000 ) ) ;
#864=CARTESIAN_POINT ( 'NONE',  ( 33.35543536254877495, -3.618985300545106920, 6.000000000000001776 ) ) ;
#872=CYLINDRICAL_SURFACE ( 'NONE', #9576, 1.999999999999986233 ) ;
#884=APPLICATION_CONTEXT ( 'automotive_design' ) ;
#890=DIRECTION ( 'NONE',  ( -0.000000000000000000, -0.000000000000000000, 1.000000000000000000 ) ) ;
#928=DIRECTION ( 'NONE',  ( -0.000000000000000000, -0.000000000000000000, 1.000000000000000000 ) ) ;
#934=ORIENTED_EDGE ( 'NONE', *, *, #1194, .T. ) ;
#1007=ORIENTED_EDGE ( 'NONE', *, *, #11900, .T. ) ;
#1010=VECTOR ( 'NONE', #6669, 1000.000000000000000 ) ;
#1016=DIRECTION ( 'NONE',  ( -1.000000000000000000, -0.000000000000000000, -0.000000000000000000 ) ) ;
#1031=ORIENTED_EDGE ( 'NONE', *, *, #11429, .F. ) ;
#1054=LINE ( 'NONE', #1990, #7758 ) ;
#1071=AXIS2_PLACEMENT_3D ( 'NONE', #14411, #9758, #14493 ) ;
#1088=ORIENTED_EDGE ( 'NONE', *, *, #8768, .F. ) ;
#1097=CARTESIAN_POINT ( 'NONE',  ( 35.35543536254876074, -3.618985300545107364, 6.000000000000001776 ) ) ;
#1135=LINE ( 'NONE', #8276, #3090 ) ;
#1137=CARTESIAN_POINT ( 'NONE',  ( 37.35543536254874653, -3.618985300545107364, 0.000000000000000000 ) ) ;
#1158=DIRECTION ( 'NONE',  ( 1.000000000000000000, 0.000000000000000000, 0.000000000000000000 ) ) ;
#1185=FACE_OUTER_BOUND ( 'NONE', #435, .T. ) ;
#1194=EDGE_CURVE ( 'NONE', #9060, #4529, #3387, .T. ) ;
#1208=ORIENTED_EDGE ( 'NONE', *, *, #1560, .T. ) ;
#1241=CYLINDRICAL_SURFACE ( 'NONE', #11950, 1.999999999999988010 ) ;
#1281=ADVANCED_FACE ( 'NONE', ( #2208 ), #4540, .F. ) ;
#1347=CARTESIAN_POINT ( 'NONE',  ( 40.52020888806953991, -24.00000000000000000, 6.000000000000000000 ) ) ;
#1353=ORIENTED_EDGE ( 'NONE', *, *, #4149, .F. ) ;
#1354=EDGE_CURVE ( 'NONE', #4630, #15067, #8348, .T. ) ;
#1409=DIRECTION ( 'NONE',  ( 1.000000000000000000, 0.000000000000000000, 0.000000000000000000 ) ) ;
#1414=FACE_BOUND ( 'NONE', #12531, .T. ) ;
#1487=DIRECTION ( 'NONE',  ( 1.000000000000000000, 0.000000000000000000, 0.000000000000000000 ) ) ;
#1558=PLANE ( 'NONE',  #8987 ) ;
#1560=EDGE_CURVE ( 'NONE', #9136, #8597, #10173, .T. ) ;
#1564=AXIS2_PLACEMENT_3D ( 'NONE', #6538, #477, #5212 ) ;
#1577=CARTESIAN_POINT ( 'NONE',  ( 0.000000000000000000, 0.000000000000000000, 0.000000000000000000 ) ) ;
#1587=CARTESIAN_POINT ( 'NONE',  ( 0.000000000000000000, 0.000000000000000000, 6.000000000000000000 ) ) ;
#1614=AXIS2_PLACEMENT_3D ( 'NONE', #4354, #928, #6764 ) ;
#1709=EDGE_CURVE ( 'NONE', #8759, #14946, #15292, .T. ) ;
#1742=ADVANCED_FACE ( 'NONE', ( #1185 ), #872, .F. ) ;
#1809=DIRECTION ( 'NONE',  ( -0.000000000000000000, -0.000000000000000000, 1.000000000000000000 ) ) ;
#1862=CIRCLE ( 'NONE', #1614, 1.999999999999988010 ) ;
#1894=ORIENTED_EDGE ( 'NONE', *, *, #8577, .T. ) ;
#1905=AXIS2_PLACEMENT_3D ( 'NONE', #12918, #14003, #6951 ) ;
#1939=FILL_AREA_STYLE_COLOUR ( '', #12281 ) ;
#1945=FACE_BOUND ( 'NONE', #3595, .T. ) ;
#1966=ORIENTED_EDGE ( 'NONE', *, *, #10962, .T. ) ;
#1990=CARTESIAN_POINT ( 'NONE',  ( 2.573385150445058223, -3.618985300545106920, 6.000000000000000000 ) ) ;
#2058=DIRECTION ( 'NONE',  ( 1.000000000000000000, 0.000000000000000000, 0.000000000000000000 ) ) ;
#2095=ORIENTED_EDGE ( 'NONE', *, *, #7161, .T. ) ;
#2137=VECTOR ( 'NONE', #1016, 1000.000000000000000 ) ;
#2150=DIRECTION ( 'NONE',  ( 1.000000000000000000, 0.000000000000000000, 0.000000000000000000 ) ) ;
#2175=ORIENTED_EDGE ( 'NONE', *, *, #11010, .F. ) ;
#2185=CARTESIAN_POINT ( 'NONE',  ( 0.000000000000000000, 0.000000000000000000, 6.000000000000000000 ) ) ;
#2206=CARTESIAN_POINT ( 'NONE',  ( 2.573385150445058223, -19.31989681812820692, 0.000000000000000000 ) ) ;
#2208=FACE_OUTER_BOUND ( 'NONE', #13929, .T. ) ;
#2224=LINE ( 'NONE', #11691, #10195 ) ;
#2322=CARTESIAN_POINT ( 'NONE',  ( 3.469446951953614189E-15, -24.00000000000000000, 6.000000000000000000 ) ) ;
#2332=DIRECTION ( 'NONE',  ( -0.000000000000000000, -0.000000000000000000, 1.000000000000000000 ) ) ;
#2347=CARTESIAN_POINT ( 'NONE',  ( 4.573385150445044900, -19.31989681812820692, 6.000000000000000000 ) ) ;
#2352=ORIENTED_EDGE ( 'NONE', *, *, #11585, .F. ) ;
#2355=DIRECTION ( 'NONE',  ( -0.000000000000000000, -0.000000000000000000, -1.000000000000000000 ) ) ;
#2357=( GEOMETRIC_REPRESENTATION_CONTEXT ( 3 ) GLOBAL_UNCERTAINTY_ASSIGNED_CONTEXT ( ( #9786 ) ) GLOBAL_UNIT_ASSIGNED_CONTEXT ( ( #5290, #6536, #5372 ) ) REPRESENTATION_CONTEXT ( 'NONE', 'WORKASPACE' ) );
#2366=VECTOR ( 'NONE', #4232, 1000.000000000000000 ) ;
#2376=LINE ( 'NONE', #46, #11606 ) ;
#2403=DIRECTION ( 'NONE',  ( -0.000000000000000000, -0.000000000000000000, -1.000000000000000000 ) ) ;
#2420=CARTESIAN_POINT ( 'NONE',  ( 35.35543536254876074, -19.31989681812820692, 6.000000000000000000 ) ) ;
#2431=ORIENTED_EDGE ( 'NONE', *, *, #11974, .F. ) ;
#2435=ORIENTED_EDGE ( 'NONE', *, *, #12919, .F. ) ;
#2445=CIRCLE ( 'NONE', #14822, 1.999999999999989564 ) ;
#2457=( NAMED_UNIT ( * ) PLANE_ANGLE_UNIT ( ) SI_UNIT ( $, .RADIAN. ) );
#2465=CARTESIAN_POINT ( 'NONE',  ( 4.573385150445044900, -19.31989681812820692, 0.000000000000000000 ) ) ;
#2482=DIRECTION ( 'NONE',  ( -0.000000000000000000, -0.000000000000000000, 1.000000000000000000 ) ) ;
#2501=VERTEX_POINT ( 'NONE', #13502 ) ;
#2587=DIRECTION ( 'NONE',  ( -0.000000000000000000, -0.000000000000000000, 1.000000000000000000 ) ) ;
#2591=DIRECTION ( 'NONE',  ( 0.000000000000000000, -1.000000000000000000, 0.000000000000000000 ) ) ;
#2596=CARTESIAN_POINT ( 'NONE',  ( 35.35543536254876074, -19.31989681812820692, 0.000000000000000000 ) ) ;
#2620=ORIENTED_EDGE ( 'NONE', *, *, #10107, .F. ) ;
#2628=AXIS2_PLACEMENT_3D ( 'NONE', #2596, #5239, #7659 ) ;
#2653=DIRECTION ( 'NONE',  ( -0.000000000000000000, -0.000000000000000000, 1.000000000000000000 ) ) ;
#2683=AXIS2_PLACEMENT_3D ( 'NONE', #15264, #9524, #7147 ) ;
#2694=LINE ( 'NONE', #14553, #12443 ) ;
#2722=FACE_BOUND ( 'NONE', #7540, .T. ) ;
#2753=ADVANCED_BREP_SHAPE_REPRESENTATION ( '', ( #5610, #285 ), #8229 ) ;
#2778=FACE_OUTER_BOUND ( 'NONE', #3285, .T. ) ;
#2874=ORIENTED_EDGE ( 'NONE', *, *, #6690, .T. ) ;
#2975=PRODUCT_DEFINITION_FORMATION_WITH_SPECIFIED_SOURCE ( 'ANY', '', #12915, .NOT_KNOWN. ) ;
#3035=DIRECTION ( 'NONE',  ( 1.000000000000000000, 0.000000000000000000, 0.000000000000000000 ) ) ;
#3090=VECTOR ( 'NONE', #13017, 1000.000000000000000 ) ;
#3099=ORIENTED_EDGE ( 'NONE', *, *, #10446, .F. ) ;
#3100=ORIENTED_EDGE ( 'NONE', *, *, #11526, .T. ) ;
#3189=DIRECTION ( 'NONE',  ( 1.000000000000000000, 0.000000000000000000, 0.000000000000000000 ) ) ;
#3190=DIRECTION ( 'NONE',  ( -1.000000000000000000, 0.000000000000000000, 0.000000000000000000 ) ) ;
#3217=CARTESIAN_POINT ( 'NONE',  ( 33.35543536254877495, -3.618985300545106920, 6.000000000000000000 ) ) ;
#3254=DIRECTION ( 'NONE',  ( 0.000000000000000000, 0.000000000000000000, 1.000000000000000000 ) ) ;
#3285=EDGE_LOOP ( 'NONE', ( #4934, #11509, #7518, #3988 ) ) ;
#3318=ORIENTED_EDGE ( 'NONE', *, *, #7161, .F. ) ;
#3319=ORIENTED_EDGE ( 'NONE', *, *, #6690, .F. ) ;
#3375=EDGE_CURVE ( 'NONE', #13570, #4529, #1135, .T. ) ;
#3387=CIRCLE ( 'NONE', #3890, 1.999999999999989564 ) ;
#3410=CARTESIAN_POINT ( 'NONE',  ( 35.35543536254876074, -3.618985300545107364, 0.000000000000000000 ) ) ;
#3423=CARTESIAN_POINT ( 'NONE',  ( 0.000000000000000000, 0.000000000000000000, 0.000000000000000000 ) ) ;
#3496=DIRECTION ( 'NONE',  ( 0.000000000000000000, 0.000000000000000000, 1.000000000000000000 ) ) ;
#3571=LINE ( 'NONE', #13045, #15181 ) ;
#3586=LINE ( 'NONE', #2185, #2137 ) ;
#3595=EDGE_LOOP ( 'NONE', ( #2874, #3705 ) ) ;
#3614=PRODUCT_CONTEXT ( 'NONE', #11997, 'mechanical' ) ;
#3648=DIRECTION ( 'NONE',  ( 1.000000000000000000, 0.000000000000000000, 0.000000000000000000 ) ) ;
#3652=ORIENTED_EDGE ( 'NONE', *, *, #5539, .F. ) ;
#3692=CARTESIAN_POINT ( 'NONE',  ( 0.000000000000000000, 0.000000000000000000, 6.000000000000000000 ) ) ;
#3705=ORIENTED_EDGE ( 'NONE', *, *, #430, .T. ) ;
#3731=FACE_BOUND ( 'NONE', #10209, .T. ) ;
#3733=FACE_OUTER_BOUND ( 'NONE', #6976, .T. ) ;
#3851=VECTOR ( 'NONE', #843, 1000.000000000000000 ) ;
#3890=AXIS2_PLACEMENT_3D ( 'NONE', #12685, #890, #2058 ) ;
#3912=CARTESIAN_POINT ( 'NONE',  ( 6.573385150445030689, -3.618985300545107364, 0.000000000000000000 ) ) ;
#3945=VERTEX_POINT ( 'NONE', #10953 ) ;
#3988=ORIENTED_EDGE ( 'NONE', *, *, #10107, .T. ) ;
#4031=ADVANCED_FACE ( 'NONE', ( #12586, #8066, #1945, #13663, #4202 ), #9220, .F. ) ;
#4131=CARTESIAN_POINT ( 'NONE',  ( 40.52020888806953991, 0.000000000000000000, 6.000000000000000000 ) ) ;
#4149=EDGE_CURVE ( 'NONE', #14022, #263, #1862, .T. ) ;
#4202=FACE_OUTER_BOUND ( 'NONE', #5744, .T. ) ;
#4208=ORIENTED_EDGE ( 'NONE', *, *, #3375, .T. ) ;
#4232=DIRECTION ( 'NONE',  ( -0.000000000000000000, -0.000000000000000000, 1.000000000000000000 ) ) ;
#4269=FACE_OUTER_BOUND ( 'NONE', #9008, .T. ) ;
#4271=DIRECTION ( 'NONE',  ( -0.000000000000000000, 0.000000000000000000, 1.000000000000000000 ) ) ;
#4284=EDGE_CURVE ( 'NONE', #2501, #14624, #10540, .T. ) ;
#4330=CARTESIAN_POINT ( 'NONE',  ( 2.573385150445055114, -19.31989681812820692, 6.000000000000001776 ) ) ;
#4354=CARTESIAN_POINT ( 'NONE',  ( 35.35543536254876074, -19.31989681812820692, 6.000000000000001776 ) ) ;
#4422=SURFACE_STYLE_FILL_AREA ( #6756 ) ;
#4514=CIRCLE ( 'NONE', #6511, 1.999999999999988010 ) ;
#4529=VERTEX_POINT ( 'NONE', #12407 ) ;
#4540=CYLINDRICAL_SURFACE ( 'NONE', #1905, 1.999999999999986233 ) ;
#4543=VERTEX_POINT ( 'NONE', #11463 ) ;
#4557=LINE ( 'NONE', #11544, #11939 ) ;
#4600=CARTESIAN_POINT ( 'NONE',  ( 35.35543536254876074, -19.31989681812820692, 6.000000000000001776 ) ) ;
#4602=MECHANICAL_DESIGN_GEOMETRIC_PRESENTATION_REPRESENTATION('',(#126),#2357);
#4628=CIRCLE ( 'NONE', #10780, 1.999999999999986233 ) ;
#4630=VERTEX_POINT ( 'NONE', #13020 ) ;
#4687=DIRECTION ( 'NONE',  ( 1.000000000000000000, 0.000000000000000000, 0.000000000000000000 ) ) ;
#4758=ADVANCED_FACE ( 'NONE', ( #10842 ), #5022, .F. ) ;
#4860=SHAPE_DEFINITION_REPRESENTATION ( #7702, #14417 ) ;
#4924=CIRCLE ( 'NONE', #2683, 1.999999999999988010 ) ;
#4931=CYLINDRICAL_SURFACE ( 'NONE', #14762, 1.999999999999986233 ) ;
#4934=ORIENTED_EDGE ( 'NONE', *, *, #8768, .T. ) ;
#4937=ORIENTED_EDGE ( 'NONE', *, *, #14536, .F. ) ;
#5022=PLANE ( 'NONE',  #10809 ) ;
#5086=FACE_OUTER_BOUND ( 'NONE', #14690, .T. ) ;
#5090=VERTEX_POINT ( 'NONE', #7333 ) ;
#5114=ORIENTED_EDGE ( 'NONE', *, *, #12919, .T. ) ;
#5126=DIRECTION ( 'NONE',  ( 0.000000000000000000, -0.000000000000000000, 1.000000000000000000 ) ) ;
#5144=DIRECTION ( 'NONE',  ( -0.000000000000000000, 0.000000000000000000, 1.000000000000000000 ) ) ;
#5185=CARTESIAN_POINT ( 'NONE',  ( 37.35543536254874653, -19.31989681812820692, 0.000000000000000000 ) ) ;
#5194=EDGE_CURVE ( 'NONE', #9136, #14122, #4628, .T. ) ;
#5212=DIRECTION ( 'NONE',  ( 1.000000000000000000, 0.000000000000000000, 0.000000000000000000 ) ) ;
#5239=DIRECTION ( 'NONE',  ( -0.000000000000000000, 0.000000000000000000, 1.000000000000000000 ) ) ;
#5290=( LENGTH_UNIT ( ) NAMED_UNIT ( * ) SI_UNIT ( .MILLI., .METRE. ) );
#5292=CYLINDRICAL_SURFACE ( 'NONE', #1564, 1.999999999999986233 ) ;
#5307=UNCERTAINTY_MEASURE_WITH_UNIT (LENGTH_MEASURE( 1.000000000000000082E-05 ), #7134, 'distance_accuracy_value', 'NONE');
#5323=CLOSED_SHELL ( 'NONE', ( #12663, #8273, #11613, #1742, #4758, #8459, #11305, #9303, #12656, #4031, #6117, #7905, #15289, #1281 ) ) ;
#5371=EDGE_CURVE ( 'NONE', #14946, #10174, #8795, .T. ) ;
#5372=( NAMED_UNIT ( * ) SI_UNIT ( $, .STERADIAN. ) SOLID_ANGLE_UNIT ( ) );
#5412=LINE ( 'NONE', #14845, #2366 ) ;
#5449=DIRECTION ( 'NONE',  ( -0.000000000000000000, 0.000000000000000000, 1.000000000000000000 ) ) ;
#5458=ORIENTED_EDGE ( 'NONE', *, *, #5960, .T. ) ;
#5465=CARTESIAN_POINT ( 'NONE',  ( 2.573385150445058223, -3.618985300545106920, 0.000000000000000000 ) ) ;
#5539=EDGE_CURVE ( 'NONE', #14624, #5090, #7770, .T. ) ;
#5542=CIRCLE ( 'NONE', #8735, 1.999999999999989564 ) ;
#5552=ORIENTED_EDGE ( 'NONE', *, *, #398, .F. ) ;
#5610=MANIFOLD_SOLID_BREP ( '\X2\00d8\X0\4.0mm Dowel Hole1', #5323 ) ;
#5659=LINE ( 'NONE', #7821, #1010 ) ;
#5704=EDGE_LOOP ( 'NONE', ( #7722, #2620, #2431, #12174 ) ) ;
#5707=EDGE_LOOP ( 'NONE', ( #15093, #14119 ) ) ;
#5744=EDGE_LOOP ( 'NONE', ( #1031, #7136, #10256, #1088 ) ) ;
#5807=CARTESIAN_POINT ( 'NONE',  ( 40.52020888806953991, -24.00000000000000000, 6.000000000000000000 ) ) ;
#5902=DIRECTION ( 'NONE',  ( -0.000000000000000000, -0.000000000000000000, 1.000000000000000000 ) ) ;
#5917=DIRECTION ( 'NONE',  ( -0.000000000000000000, -0.000000000000000000, 1.000000000000000000 ) ) ;
#5954=LINE ( 'NONE', #1347, #9192 ) ;
#5960=EDGE_CURVE ( 'NONE', #12176, #14022, #5412, .T. ) ;
#5965=ORIENTED_EDGE ( 'NONE', *, *, #8577, .F. ) ;
#5979=ORIENTED_EDGE ( 'NONE', *, *, #4149, .T. ) ;
#6117=ADVANCED_FACE ( 'NONE', ( #10736 ), #4931, .F. ) ;
#6172=FACE_OUTER_BOUND ( 'NONE', #12363, .T. ) ;
#6279=CARTESIAN_POINT ( 'NONE',  ( 0.000000000000000000, 0.000000000000000000, 6.000000000000000000 ) ) ;
#6281=DIRECTION ( 'NONE',  ( -0.000000000000000000, 1.000000000000000000, -0.000000000000000000 ) ) ;
#6321=CARTESIAN_POINT ( 'NONE',  ( 4.573385150445044900, -3.618985300545107364, 0.000000000000000000 ) ) ;
#6379=EDGE_LOOP ( 'NONE', ( #14462, #628, #820, #12603 ) ) ;
#6511=AXIS2_PLACEMENT_3D ( 'NONE', #3410, #8219, #10539 ) ;
#6536=( NAMED_UNIT ( * ) PLANE_ANGLE_UNIT ( ) SI_UNIT ( $, .RADIAN. ) );
#6538=CARTESIAN_POINT ( 'NONE',  ( 4.573385150445044900, -3.618985300545107364, 6.000000000000000000 ) ) ;
#6608=EDGE_CURVE ( 'NONE', #5090, #12114, #3586, .T. ) ;
#6667=ORIENTED_EDGE ( 'NONE', *, *, #4284, .T. ) ;
#6669=DIRECTION ( 'NONE',  ( -0.000000000000000000, -0.000000000000000000, 1.000000000000000000 ) ) ;
#6690=EDGE_CURVE ( 'NONE', #12176, #12493, #406, .T. ) ;
#6756=FILL_AREA_STYLE ('',( #1939 ) ) ;
#6764=DIRECTION ( 'NONE',  ( 1.000000000000000000, 0.000000000000000000, 0.000000000000000000 ) ) ;
#6855=AXIS2_PLACEMENT_3D ( 'NONE', #6321, #10013, #3035 ) ;
#6865=ORIENTED_EDGE ( 'NONE', *, *, #9121, .T. ) ;
#6951=DIRECTION ( 'NONE',  ( 1.000000000000000000, 0.000000000000000000, 0.000000000000000000 ) ) ;
#6975=ORIENTED_EDGE ( 'NONE', *, *, #8364, .T. ) ;
#6976=EDGE_LOOP ( 'NONE', ( #4937, #3319, #5458, #5979 ) ) ;
#7100=DIRECTION ( 'NONE',  ( -0.000000000000000000, -0.000000000000000000, 1.000000000000000000 ) ) ;
#7134=( LENGTH_UNIT ( ) NAMED_UNIT ( * ) SI_UNIT ( .MILLI., .METRE. ) );
#7136=ORIENTED_EDGE ( 'NONE', *, *, #1354, .F. ) ;
#7147=DIRECTION ( 'NONE',  ( 1.000000000000000000, 0.000000000000000000, 0.000000000000000000 ) ) ;
#7161=EDGE_CURVE ( 'NONE', #14122, #9136, #14289, .T. ) ;
#7203=DIRECTION ( 'NONE',  ( 1.000000000000000000, 0.000000000000000000, 0.000000000000000000 ) ) ;
#7212=EDGE_LOOP ( 'NONE', ( #7706, #3318, #1007, #1966 ) ) ;
#7215=DIRECTION ( 'NONE',  ( -0.000000000000000000, 0.000000000000000000, 1.000000000000000000 ) ) ;
#7229=DIRECTION ( 'NONE',  ( 1.000000000000000000, 0.000000000000000000, 0.000000000000000000 ) ) ;
#7317=CYLINDRICAL_SURFACE ( 'NONE', #8864, 1.999999999999988010 ) ;
#7333=CARTESIAN_POINT ( 'NONE',  ( 40.52020888806953991, 0.000000000000000000, 6.000000000000000000 ) ) ;
#7335=DIRECTION ( 'NONE',  ( 1.000000000000000000, 0.000000000000000000, 0.000000000000000000 ) ) ;
#7428=PRODUCT_DEFINITION ( 'UNKNOWN', '', #2975, #7642 ) ;
#7455=DIRECTION ( 'NONE',  ( -0.000000000000000000, 0.000000000000000000, 1.000000000000000000 ) ) ;
#7518=ORIENTED_EDGE ( 'NONE', *, *, #4284, .F. ) ;
#7521=CIRCLE ( 'NONE', #10471, 1.999999999999988010 ) ;
#7540=EDGE_LOOP ( 'NONE', ( #1353, #2175 ) ) ;
#7576=DIRECTION ( 'NONE',  ( 0.000000000000000000, -0.000000000000000000, -1.000000000000000000 ) ) ;
#7642=PRODUCT_DEFINITION_CONTEXT ( 'detailed design', #884, 'design' ) ;
#7659=DIRECTION ( 'NONE',  ( 1.000000000000000000, 0.000000000000000000, 0.000000000000000000 ) ) ;
#7695=SURFACE_STYLE_USAGE ( .BOTH. , #15033 ) ;
#7702=PRODUCT_DEFINITION_SHAPE ( 'NONE', 'NONE',  #7428 ) ;
#7706=ORIENTED_EDGE ( 'NONE', *, *, #1560, .F. ) ;
#7722=ORIENTED_EDGE ( 'NONE', *, *, #11429, .T. ) ;
#7754=CARTESIAN_POINT ( 'NONE',  ( 4.573385150445044900, -19.31989681812820692, 6.000000000000001776 ) ) ;
#7758=VECTOR ( 'NONE', #828, 1000.000000000000000 ) ;
#7764=ORIENTED_EDGE ( 'NONE', *, *, #1354, .T. ) ;
#7770=LINE ( 'NONE', #11477, #3851 ) ;
#7811=CARTESIAN_POINT ( 'NONE',  ( 4.573385150445044900, -19.31989681812820692, 6.000000000000001776 ) ) ;
#7821=CARTESIAN_POINT ( 'NONE',  ( 33.35543536254877495, -19.31989681812820692, 6.000000000000000000 ) ) ;
#7890=ORIENTED_EDGE ( 'NONE', *, *, #10730, .F. ) ;
#7905=ADVANCED_FACE ( 'NONE', ( #3733 ), #7317, .F. ) ;
#7955=ORIENTED_EDGE ( 'NONE', *, *, #11585, .T. ) ;
#7998=DIRECTION ( 'NONE',  ( 1.000000000000000000, 0.000000000000000000, 0.000000000000000000 ) ) ;
#8001=CARTESIAN_POINT ( 'NONE',  ( 33.35543536254877495, -19.31989681812820692, 0.000000000000000000 ) ) ;
#8052=EDGE_LOOP ( 'NONE', ( #13483, #10154 ) ) ;
#8066=FACE_BOUND ( 'NONE', #5707, .T. ) ;
#8131=AXIS2_PLACEMENT_3D ( 'NONE', #461, #599, #5126 ) ;
#8187=EDGE_CURVE ( 'NONE', #8759, #3945, #452, .T. ) ;
#8219=DIRECTION ( 'NONE',  ( -0.000000000000000000, 0.000000000000000000, 1.000000000000000000 ) ) ;
#8229=( GEOMETRIC_REPRESENTATION_CONTEXT ( 3 ) GLOBAL_UNCERTAINTY_ASSIGNED_CONTEXT ( ( #5307 ) ) GLOBAL_UNIT_ASSIGNED_CONTEXT ( ( #7134, #2457, #10604 ) ) REPRESENTATION_CONTEXT ( 'NONE', 'WORKASPACE' ) );
#8243=DIRECTION ( 'NONE',  ( -0.000000000000000000, -0.000000000000000000, 1.000000000000000000 ) ) ;
#8264=ORIENTED_EDGE ( 'NONE', *, *, #6608, .T. ) ;
#8273=ADVANCED_FACE ( 'NONE', ( #4269 ), #11399, .F. ) ;
#8276=CARTESIAN_POINT ( 'NONE',  ( 6.573385150445030689, -3.618985300545107364, 6.000000000000000000 ) ) ;
#8326=DIRECTION ( 'NONE',  ( -0.000000000000000000, -0.000000000000000000, 1.000000000000000000 ) ) ;
#8347=VECTOR ( 'NONE', #1809, 1000.000000000000000 ) ;
#8348=LINE ( 'NONE', #10657, #14041 ) ;
#8364=EDGE_CURVE ( 'NONE', #10174, #14946, #4924, .T. ) ;
#8388=EDGE_LOOP ( 'NONE', ( #7955, #13355 ) ) ;
#8400=DIRECTION ( 'NONE',  ( 1.000000000000000000, 0.000000000000000000, 0.000000000000000000 ) ) ;
#8457=FACE_OUTER_BOUND ( 'NONE', #6379, .T. ) ;
#8459=ADVANCED_FACE ( 'NONE', ( #2778 ), #11008, .F. ) ;
#8461=FACE_BOUND ( 'NONE', #8052, .T. ) ;
#8577=EDGE_CURVE ( 'NONE', #8597, #11302, #2445, .T. ) ;
#8597=VERTEX_POINT ( 'NONE', #4330 ) ;
#8608=DIRECTION ( 'NONE',  ( 1.000000000000000000, 0.000000000000000000, 0.000000000000000000 ) ) ;
#8619=DIRECTION ( 'NONE',  ( 1.000000000000000000, 0.000000000000000000, 0.000000000000000000 ) ) ;
#8628=AXIS2_PLACEMENT_3D ( 'NONE', #766, #5917, #1158 ) ;
#8687=CARTESIAN_POINT ( 'NONE',  ( 37.35543536254874653, -19.31989681812820692, 6.000000000000001776 ) ) ;
#8735=AXIS2_PLACEMENT_3D ( 'NONE', #10380, #12717, #12642 ) ;
#8738=EDGE_LOOP ( 'NONE', ( #11013, #9457, #11800, #8896 ) ) ;
#8759=VERTEX_POINT ( 'NONE', #1137 ) ;
#8768=EDGE_CURVE ( 'NONE', #4543, #726, #2376, .T. ) ;
#8795=CIRCLE ( 'NONE', #12309, 1.999999999999988010 ) ;
#8861=ORIENTED_EDGE ( 'NONE', *, *, #9810, .T. ) ;
#8864=AXIS2_PLACEMENT_3D ( 'NONE', #2420, #2653, #9694 ) ;
#8896=ORIENTED_EDGE ( 'NONE', *, *, #5960, .F. ) ;
#8987=AXIS2_PLACEMENT_3D ( 'NONE', #12119, #236, #1487 ) ;
#9008=EDGE_LOOP ( 'NONE', ( #3099, #6865, #6975, #9827 ) ) ;
#9014=LINE ( 'NONE', #10326, #13194 ) ;
#9060=VERTEX_POINT ( 'NONE', #11293 ) ;
#9065=ORIENTED_EDGE ( 'NONE', *, *, #10730, .T. ) ;
#9069=AXIS2_PLACEMENT_3D ( 'NONE', #12121, #5144, #8619 ) ;
#9121=EDGE_CURVE ( 'NONE', #3945, #10174, #11523, .T. ) ;
#9136=VERTEX_POINT ( 'NONE', #2206 ) ;
#9192=VECTOR ( 'NONE', #2355, 1000.000000000000000 ) ;
#9220=PLANE ( 'NONE',  #11773 ) ;
#9243=CIRCLE ( 'NONE', #11234, 1.999999999999986233 ) ;
#9245=CARTESIAN_POINT ( 'NONE',  ( 37.35543536254874653, -3.618985300545107364, 6.000000000000000000 ) ) ;
#9289=ORIENTED_EDGE ( 'NONE', *, *, #12013, .T. ) ;
#9303=ADVANCED_FACE ( 'NONE', ( #5086 ), #13387, .F. ) ;
#9439=ORIENTED_EDGE ( 'NONE', *, *, #11900, .F. ) ;
#9457=ORIENTED_EDGE ( 'NONE', *, *, #14536, .T. ) ;
#9524=DIRECTION ( 'NONE',  ( -0.000000000000000000, -0.000000000000000000, 1.000000000000000000 ) ) ;
#9539=DIRECTION ( 'NONE',  ( 1.000000000000000000, 0.000000000000000000, 0.000000000000000000 ) ) ;
#9576=AXIS2_PLACEMENT_3D ( 'NONE', #2347, #7100, #4687 ) ;
#9655=DIRECTION ( 'NONE',  ( 1.000000000000000000, 1.445602896647339163E-16, -0.000000000000000000 ) ) ;
#9694=DIRECTION ( 'NONE',  ( 1.000000000000000000, 0.000000000000000000, 0.000000000000000000 ) ) ;
#9758=DIRECTION ( 'NONE',  ( -0.000000000000000000, -0.000000000000000000, 1.000000000000000000 ) ) ;
#9786=UNCERTAINTY_MEASURE_WITH_UNIT (LENGTH_MEASURE( 1.000000000000000082E-05 ), #5290, 'distance_accuracy_value', 'NONE');
#9810=EDGE_CURVE ( 'NONE', #14624, #726, #5954, .T. ) ;
#9817=CIRCLE ( 'NONE', #6855, 1.999999999999986233 ) ;
#9827=ORIENTED_EDGE ( 'NONE', *, *, #1709, .F. ) ;
#9913=CYLINDRICAL_SURFACE ( 'NONE', #1071, 1.999999999999988010 ) ;
#9974=CIRCLE ( 'NONE', #13939, 1.999999999999989564 ) ;
#9998=VECTOR ( 'NONE', #10349, 1000.000000000000000 ) ;
#10013=DIRECTION ( 'NONE',  ( -0.000000000000000000, 0.000000000000000000, 1.000000000000000000 ) ) ;
#10103=AXIS2_PLACEMENT_3D ( 'NONE', #12645, #5449, #10310 ) ;
#10107=EDGE_CURVE ( 'NONE', #2501, #4543, #9014, .T. ) ;
#10154=ORIENTED_EDGE ( 'NONE', *, *, #8364, .F. ) ;
#10173=LINE ( 'NONE', #13839, #8347 ) ;
#10174=VERTEX_POINT ( 'NONE', #864 ) ;
#10195=VECTOR ( 'NONE', #14100, 1000.000000000000000 ) ;
#10209=EDGE_LOOP ( 'NONE', ( #2435, #14302 ) ) ;
#10232=VERTEX_POINT ( 'NONE', #5465 ) ;
#10235=AXIS2_PLACEMENT_3D ( 'NONE', #4131, #3190, #3254 ) ;
#10256=ORIENTED_EDGE ( 'NONE', *, *, #12013, .F. ) ;
#10296=ORIENTED_EDGE ( 'NONE', *, *, #10962, .F. ) ;
#10310=DIRECTION ( 'NONE',  ( 1.000000000000000000, 0.000000000000000000, 0.000000000000000000 ) ) ;
#10326=CARTESIAN_POINT ( 'NONE',  ( 3.469446951953614189E-15, -24.00000000000000000, 6.000000000000000000 ) ) ;
#10349=DIRECTION ( 'NONE',  ( -0.000000000000000000, -0.000000000000000000, 1.000000000000000000 ) ) ;
#10380=CARTESIAN_POINT ( 'NONE',  ( 4.573385150445044900, -3.618985300545107364, 6.000000000000001776 ) ) ;
#10446=EDGE_CURVE ( 'NONE', #3945, #8759, #4514, .T. ) ;
#10471=AXIS2_PLACEMENT_3D ( 'NONE', #4600, #8243, #10565 ) ;
#10539=DIRECTION ( 'NONE',  ( 1.000000000000000000, 0.000000000000000000, 0.000000000000000000 ) ) ;
#10540=LINE ( 'NONE', #2322, #13038 ) ;
#10565=DIRECTION ( 'NONE',  ( 1.000000000000000000, 0.000000000000000000, 0.000000000000000000 ) ) ;
#10604=( NAMED_UNIT ( * ) SI_UNIT ( $, .STERADIAN. ) SOLID_ANGLE_UNIT ( ) );
#10657=CARTESIAN_POINT ( 'NONE',  ( 0.000000000000000000, 0.000000000000000000, 0.000000000000000000 ) ) ;
#10671=AXIS2_PLACEMENT_3D ( 'NONE', #1587, #2591, #7576 ) ;
#10676=ORIENTED_EDGE ( 'NONE', *, *, #6608, .F. ) ;
#10678=SHAPE_REPRESENTATION_RELATIONSHIP ( 'NONE' , 'NONE' ,  #14417, #2753 ) ;
#10730=EDGE_CURVE ( 'NONE', #10232, #9060, #1054, .T. ) ;
#10736=FACE_OUTER_BOUND ( 'NONE', #7212, .T. ) ;
#10762=DIRECTION ( 'NONE',  ( -1.445602896647339163E-16, 1.000000000000000000, 0.000000000000000000 ) ) ;
#10780=AXIS2_PLACEMENT_3D ( 'NONE', #14828, #12520, #7998 ) ;
#10809=AXIS2_PLACEMENT_3D ( 'NONE', #6279, #9655, #10762 ) ;
#10842=FACE_OUTER_BOUND ( 'NONE', #5704, .T. ) ;
#10865=FACE_OUTER_BOUND ( 'NONE', #8738, .T. ) ;
#10953=CARTESIAN_POINT ( 'NONE',  ( 33.35543536254877495, -3.618985300545106920, 0.000000000000000000 ) ) ;
#10962=EDGE_CURVE ( 'NONE', #11302, #8597, #9974, .T. ) ;
#11008=PLANE ( 'NONE',  #8131 ) ;
#11010=EDGE_CURVE ( 'NONE', #263, #14022, #7521, .T. ) ;
#11012=CARTESIAN_POINT ( 'NONE',  ( 4.573385150445044900, -3.618985300545107364, 0.000000000000000000 ) ) ;
#11013=ORIENTED_EDGE ( 'NONE', *, *, #430, .F. ) ;
#11234=AXIS2_PLACEMENT_3D ( 'NONE', #11012, #7455, #8608 ) ;
#11293=CARTESIAN_POINT ( 'NONE',  ( 2.573385150445055114, -3.618985300545106920, 6.000000000000001776 ) ) ;
#11302=VERTEX_POINT ( 'NONE', #12727 ) ;
#11305=ADVANCED_FACE ( 'NONE', ( #14964 ), #12511, .F. ) ;
#11399=CYLINDRICAL_SURFACE ( 'NONE', #8628, 1.999999999999988010 ) ;
#11429=EDGE_CURVE ( 'NONE', #15067, #4543, #15271, .T. ) ;
#11463=CARTESIAN_POINT ( 'NONE',  ( 3.469446951953614189E-15, -24.00000000000000000, 0.000000000000000000 ) ) ;
#11477=CARTESIAN_POINT ( 'NONE',  ( 40.52020888806953991, 0.000000000000000000, 6.000000000000000000 ) ) ;
#11509=ORIENTED_EDGE ( 'NONE', *, *, #9810, .F. ) ;
#11523=LINE ( 'NONE', #3217, #9998 ) ;
#11526=EDGE_CURVE ( 'NONE', #5090, #4630, #3571, .T. ) ;
#11544=CARTESIAN_POINT ( 'NONE',  ( 6.573385150445030689, -19.31989681812820692, 6.000000000000000000 ) ) ;
#11585=EDGE_CURVE ( 'NONE', #13570, #10232, #9243, .T. ) ;
#11606=VECTOR ( 'NONE', #7203, 1000.000000000000000 ) ;
#11613=ADVANCED_FACE ( 'NONE', ( #10865 ), #9913, .F. ) ;
#11678=ORIENTED_EDGE ( 'NONE', *, *, #5194, .T. ) ;
#11691=CARTESIAN_POINT ( 'NONE',  ( 0.000000000000000000, 0.000000000000000000, 6.000000000000000000 ) ) ;
#11724=ORIENTED_EDGE ( 'NONE', *, *, #713, .F. ) ;
#11726=CARTESIAN_POINT ( 'NONE',  ( 35.35543536254876074, -3.618985300545107364, 6.000000000000000000 ) ) ;
#11773=AXIS2_PLACEMENT_3D ( 'NONE', #13743, #4271, #3189 ) ;
#11800=ORIENTED_EDGE ( 'NONE', *, *, #11010, .T. ) ;
#11900=EDGE_CURVE ( 'NONE', #14122, #11302, #4557, .T. ) ;
#11939=VECTOR ( 'NONE', #5902, 1000.000000000000000 ) ;
#11950=AXIS2_PLACEMENT_3D ( 'NONE', #11726, #2332, #7229 ) ;
#11974=EDGE_CURVE ( 'NONE', #12114, #2501, #2224, .T. ) ;
#11993=DIRECTION ( 'NONE',  ( -0.000000000000000000, -0.000000000000000000, -1.000000000000000000 ) ) ;
#11997=APPLICATION_CONTEXT ( 'automotive_design' ) ;
#12013=EDGE_CURVE ( 'NONE', #726, #4630, #2694, .T. ) ;
#12058=CARTESIAN_POINT ( 'NONE',  ( 37.35543536254874653, -3.618985300545107364, 6.000000000000001776 ) ) ;
#12114=VERTEX_POINT ( 'NONE', #586 ) ;
#12119=CARTESIAN_POINT ( 'NONE',  ( 0.000000000000000000, 0.000000000000000000, 6.000000000000000000 ) ) ;
#12121=CARTESIAN_POINT ( 'NONE',  ( 35.35543536254876074, -19.31989681812820692, 0.000000000000000000 ) ) ;
#12174=ORIENTED_EDGE ( 'NONE', *, *, #398, .T. ) ;
#12176=VERTEX_POINT ( 'NONE', #5185 ) ;
#12281=COLOUR_RGB ( '', 0.31764706, 0.68627451, 0.89019608) ;
#12309=AXIS2_PLACEMENT_3D ( 'NONE', #1097, #2482, #9539 ) ;
#12340=ORIENTED_EDGE ( 'NONE', *, *, #11526, .F. ) ;
#12347=PRESENTATION_STYLE_ASSIGNMENT (( #7695 ) ) ;
#12363=EDGE_LOOP ( 'NONE', ( #12886, #6667, #14821, #8264 ) ) ;
#12407=CARTESIAN_POINT ( 'NONE',  ( 6.573385150445034242, -3.618985300545107364, 6.000000000000001776 ) ) ;
#12443=VECTOR ( 'NONE', #6281, 1000.000000000000000 ) ;
#12493=VERTEX_POINT ( 'NONE', #8001 ) ;
#12511=PLANE ( 'NONE',  #10235 ) ;
#12520=DIRECTION ( 'NONE',  ( -0.000000000000000000, 0.000000000000000000, 1.000000000000000000 ) ) ;
#12531=EDGE_LOOP ( 'NONE', ( #10296, #5965 ) ) ;
#12551=CARTESIAN_POINT ( 'NONE',  ( 33.35543536254877495, -19.31989681812820692, 6.000000000000001776 ) ) ;
#12586=FACE_BOUND ( 'NONE', #8388, .T. ) ;
#12603=ORIENTED_EDGE ( 'NONE', *, *, #5371, .T. ) ;
#12642=DIRECTION ( 'NONE',  ( 1.000000000000000000, 0.000000000000000000, 0.000000000000000000 ) ) ;
#12645=CARTESIAN_POINT ( 'NONE',  ( 35.35543536254876074, -3.618985300545107364, 0.000000000000000000 ) ) ;
#12656=ADVANCED_FACE ( 'NONE', ( #3731, #8461, #2722, #1414, #6172 ), #1558, .T. ) ;
#12663=ADVANCED_FACE ( 'NONE', ( #397 ), #5292, .F. ) ;
#12685=CARTESIAN_POINT ( 'NONE',  ( 4.573385150445044900, -3.618985300545107364, 6.000000000000001776 ) ) ;
#12713=CARTESIAN_POINT ( 'NONE',  ( 6.573385150445030689, -19.31989681812820692, 0.000000000000000000 ) ) ;
#12717=DIRECTION ( 'NONE',  ( -0.000000000000000000, -0.000000000000000000, 1.000000000000000000 ) ) ;
#12727=CARTESIAN_POINT ( 'NONE',  ( 6.573385150445034242, -19.31989681812820692, 6.000000000000001776 ) ) ;
#12738=DIRECTION ( 'NONE',  ( -0.000000000000000000, -0.000000000000000000, -1.000000000000000000 ) ) ;
#12886=ORIENTED_EDGE ( 'NONE', *, *, #11974, .T. ) ;
#12915=PRODUCT ( 'Part1', 'Part1', '', ( #3614 ) ) ;
#12918=CARTESIAN_POINT ( 'NONE',  ( 4.573385150445044900, -3.618985300545107364, 6.000000000000000000 ) ) ;
#12919=EDGE_CURVE ( 'NONE', #4529, #9060, #5542, .T. ) ;
#13017=DIRECTION ( 'NONE',  ( -0.000000000000000000, -0.000000000000000000, 1.000000000000000000 ) ) ;
#13020=CARTESIAN_POINT ( 'NONE',  ( 40.52020888806953991, 0.000000000000000000, 0.000000000000000000 ) ) ;
#13038=VECTOR ( 'NONE', #3648, 1000.000000000000000 ) ;
#13045=CARTESIAN_POINT ( 'NONE',  ( 40.52020888806953991, 0.000000000000000000, 6.000000000000000000 ) ) ;
#13194=VECTOR ( 'NONE', #12738, 1000.000000000000000 ) ;
#13355=ORIENTED_EDGE ( 'NONE', *, *, #713, .T. ) ;
#13387=PLANE ( 'NONE',  #10671 ) ;
#13483=ORIENTED_EDGE ( 'NONE', *, *, #5371, .F. ) ;
#13502=CARTESIAN_POINT ( 'NONE',  ( 3.469446951953614189E-15, -24.00000000000000000, 6.000000000000000000 ) ) ;
#13570=VERTEX_POINT ( 'NONE', #3912 ) ;
#13580=EDGE_LOOP ( 'NONE', ( #9289, #12340, #3652, #8861 ) ) ;
#13663=FACE_BOUND ( 'NONE', #297, .T. ) ;
#13743=CARTESIAN_POINT ( 'NONE',  ( 0.000000000000000000, 0.000000000000000000, 0.000000000000000000 ) ) ;
#13839=CARTESIAN_POINT ( 'NONE',  ( 2.573385150445058223, -19.31989681812820692, 6.000000000000000000 ) ) ;
#13929=EDGE_LOOP ( 'NONE', ( #7890, #2352, #4208, #5114 ) ) ;
#13936=DIRECTION ( 'NONE',  ( -0.000000000000000000, -0.000000000000000000, 1.000000000000000000 ) ) ;
#13939=AXIS2_PLACEMENT_3D ( 'NONE', #7811, #8326, #8400 ) ;
#14003=DIRECTION ( 'NONE',  ( -0.000000000000000000, -0.000000000000000000, 1.000000000000000000 ) ) ;
#14014=CIRCLE ( 'NONE', #2628, 1.999999999999988010 ) ;
#14022=VERTEX_POINT ( 'NONE', #8687 ) ;
#14041=VECTOR ( 'NONE', #15231, 1000.000000000000000 ) ;
#14052=VECTOR ( 'NONE', #15212, 1000.000000000000000 ) ;
#14100=DIRECTION ( 'NONE',  ( 1.445602896647339163E-16, -1.000000000000000000, 0.000000000000000000 ) ) ;
#14119=ORIENTED_EDGE ( 'NONE', *, *, #10446, .T. ) ;
#14122=VERTEX_POINT ( 'NONE', #12713 ) ;
#14271=CARTESIAN_POINT ( 'NONE',  ( 0.000000000000000000, 0.000000000000000000, 0.000000000000000000 ) ) ;
#14289=CIRCLE ( 'NONE', #168, 1.999999999999986233 ) ;
#14302=ORIENTED_EDGE ( 'NONE', *, *, #1194, .F. ) ;
#14313=LINE ( 'NONE', #3692, #14510 ) ;
#14411=CARTESIAN_POINT ( 'NONE',  ( 35.35543536254876074, -19.31989681812820692, 6.000000000000000000 ) ) ;
#14417=SHAPE_REPRESENTATION ( 'Part1', ( #285 ), #8229 ) ;
#14462=ORIENTED_EDGE ( 'NONE', *, *, #9121, .F. ) ;
#14493=DIRECTION ( 'NONE',  ( 1.000000000000000000, 0.000000000000000000, 0.000000000000000000 ) ) ;
#14510=VECTOR ( 'NONE', #11993, 1000.000000000000000 ) ;
#14536=EDGE_CURVE ( 'NONE', #12493, #263, #5659, .T. ) ;
#14553=CARTESIAN_POINT ( 'NONE',  ( 40.52020888806953991, 0.000000000000000000, 0.000000000000000000 ) ) ;
#14624=VERTEX_POINT ( 'NONE', #5807 ) ;
#14643=ORIENTED_EDGE ( 'NONE', *, *, #3375, .F. ) ;
#14690=EDGE_LOOP ( 'NONE', ( #7764, #5552, #10676, #3100 ) ) ;
#14703=ORIENTED_EDGE ( 'NONE', *, *, #5194, .F. ) ;
#14762=AXIS2_PLACEMENT_3D ( 'NONE', #24, #2587, #7335 ) ;
#14821=ORIENTED_EDGE ( 'NONE', *, *, #5539, .T. ) ;
#14822=AXIS2_PLACEMENT_3D ( 'NONE', #7754, #13936, #2150 ) ;
#14828=CARTESIAN_POINT ( 'NONE',  ( 4.573385150445044900, -19.31989681812820692, 0.000000000000000000 ) ) ;
#14845=CARTESIAN_POINT ( 'NONE',  ( 37.35543536254874653, -19.31989681812820692, 6.000000000000000000 ) ) ;
#14946=VERTEX_POINT ( 'NONE', #12058 ) ;
#14964=FACE_OUTER_BOUND ( 'NONE', #13580, .T. ) ;
#15033=SURFACE_SIDE_STYLE ('',( #4422 ) ) ;
#15067=VERTEX_POINT ( 'NONE', #1577 ) ;
#15093=ORIENTED_EDGE ( 'NONE', *, *, #8187, .T. ) ;
#15181=VECTOR ( 'NONE', #2403, 1000.000000000000000 ) ;
#15192=DIRECTION ( 'NONE',  ( 1.445602896647339163E-16, -1.000000000000000000, 0.000000000000000000 ) ) ;
#15212=DIRECTION ( 'NONE',  ( -0.000000000000000000, -0.000000000000000000, 1.000000000000000000 ) ) ;
#15231=DIRECTION ( 'NONE',  ( -1.000000000000000000, -0.000000000000000000, -0.000000000000000000 ) ) ;
#15264=CARTESIAN_POINT ( 'NONE',  ( 35.35543536254876074, -3.618985300545107364, 6.000000000000001776 ) ) ;
#15271=LINE ( 'NONE', #14271, #74 ) ;
#15289=ADVANCED_FACE ( 'NONE', ( #8457 ), #1241, .F. ) ;
#15292=LINE ( 'NONE', #9245, #14052 ) ;
ENDSEC;
END-ISO-10303-21;
